ISO-10303-21;
HEADER;
/* Generated by software containing ST-Developer
 * from STEP Tools, Inc. (www.steptools.com) 
 */

FILE_DESCRIPTION(
/* description */ ('Union bypass pipe loop'),
/* implementation_level */ '2;1');

FILE_NAME(
/* name */ 'M4x10 Cap Screw.step',
/* time_stamp */ '2026-10-27T21:00:29-07:00',
/* author */ (''),
/* organization */ (''),
/* preprocessor_version */ 'ST-DEVELOPER v20.2',
/* originating_system */ 'Autodesk Translation Framework v15.17.0.0',
/* authorisation */ '');

FILE_SCHEMA (('AUTOMOTIVE_DESIGN { 1 0 10303 214 3 1 1 }'));
ENDSEC;

DATA;
#10=MECHANICAL_DESIGN_GEOMETRIC_PRESENTATION_REPRESENTATION('',(#476),#10095);
#369=CONICAL_SURFACE('',#6600,0.325,0.785398163397448);
#370=CONICAL_SURFACE('',#6604,0.335,0.785398163397448);
#371=CONICAL_SURFACE('',#6608,0.21,0.463647609000806);
#375=ORIENTED_CLOSED_SHELL('',*,#5550,.F.);
#379=BREP_WITH_VOIDS('Body1',#5551,(#375));
#412=SHAPE_REPRESENTATION_RELATIONSHIP('SRR','None',#10282,#444);
#444=ADVANCED_BREP_SHAPE_REPRESENTATION('',(#379),#10094);
#476=STYLED_ITEM('',(#10507),#379);
#634=FACE_BOUND('',#1620,.T.);
#824=PLANE('',#6588);
#825=PLANE('',#6589);
#826=PLANE('',#6590);
#827=PLANE('',#6591);
#828=PLANE('',#6592);
#829=PLANE('',#6593);
#830=PLANE('',#6594);
#831=PLANE('',#6595);
#832=PLANE('',#6596);
#833=PLANE('',#6598);
#834=PLANE('',#6606);
#1151=FACE_OUTER_BOUND('',#1606,.T.);
#1152=FACE_OUTER_BOUND('',#1607,.T.);
#1153=FACE_OUTER_BOUND('',#1608,.T.);
#1154=FACE_OUTER_BOUND('',#1609,.T.);
#1155=FACE_OUTER_BOUND('',#1610,.T.);
#1156=FACE_OUTER_BOUND('',#1611,.T.);
#1157=FACE_OUTER_BOUND('',#1612,.T.);
#1158=FACE_OUTER_BOUND('',#1613,.T.);
#1159=FACE_OUTER_BOUND('',#1614,.T.);
#1160=FACE_OUTER_BOUND('',#1615,.T.);
#1161=FACE_OUTER_BOUND('',#1616,.T.);
#1162=FACE_OUTER_BOUND('',#1617,.T.);
#1163=FACE_OUTER_BOUND('',#1618,.T.);
#1164=FACE_OUTER_BOUND('',#1619,.T.);
#1165=FACE_OUTER_BOUND('',#1621,.T.);
#1166=FACE_OUTER_BOUND('',#1622,.T.);
#1606=EDGE_LOOP('',(#5020,#5021,#5022,#5023));
#1607=EDGE_LOOP('',(#5024,#5025,#5026,#5027));
#1608=EDGE_LOOP('',(#5028,#5029,#5030,#5031));
#1609=EDGE_LOOP('',(#5032,#5033,#5034,#5035));
#1610=EDGE_LOOP('',(#5036,#5037,#5038,#5039));
#1611=EDGE_LOOP('',(#5040,#5041,#5042,#5043));
#1612=EDGE_LOOP('',(#5044,#5045,#5046,#5047,#5048,#5049));
#1613=EDGE_LOOP('',(#5050,#5051,#5052,#5053,#5054,#5055));
#1614=EDGE_LOOP('',(#5056));
#1615=EDGE_LOOP('',(#5057));
#1616=EDGE_LOOP('',(#5058,#5059,#5060,#5061));
#1617=EDGE_LOOP('',(#5062,#5063,#5064,#5065));
#1618=EDGE_LOOP('',(#5066,#5067,#5068,#5069));
#1619=EDGE_LOOP('',(#5070));
#1620=EDGE_LOOP('',(#5071));
#1621=EDGE_LOOP('',(#5072,#5073,#5074,#5075));
#1622=EDGE_LOOP('',(#5076,#5077,#5078,#5079));
#1976=LINE('',#9952,#2352);
#1977=LINE('',#9954,#2353);
#1978=LINE('',#9956,#2354);
#1979=LINE('',#9957,#2355);
#1980=LINE('',#9960,#2356);
#1981=LINE('',#9962,#2357);
#1982=LINE('',#9963,#2358);
#1983=LINE('',#9966,#2359);
#1984=LINE('',#9968,#2360);
#1985=LINE('',#9969,#2361);
#1986=LINE('',#9972,#2362);
#1987=LINE('',#9974,#2363);
#1988=LINE('',#9975,#2364);
#1989=LINE('',#9978,#2365);
#1990=LINE('',#9980,#2366);
#1991=LINE('',#9981,#2367);
#1992=LINE('',#9983,#2368);
#1993=LINE('',#9984,#2369);
#1994=LINE('',#9996,#2370);
#1995=LINE('',#10000,#2371);
#1996=LINE('',#10004,#2372);
#1997=LINE('',#10011,#2373);
#1998=LINE('',#10013,#2374);
#2352=VECTOR('',#8340,1.);
#2353=VECTOR('',#8341,1.);
#2354=VECTOR('',#8342,1.);
#2355=VECTOR('',#8343,1.);
#2356=VECTOR('',#8346,1.);
#2357=VECTOR('',#8347,1.);
#2358=VECTOR('',#8348,1.);
#2359=VECTOR('',#8351,1.);
#2360=VECTOR('',#8352,1.);
#2361=VECTOR('',#8353,1.);
#2362=VECTOR('',#8356,1.);
#2363=VECTOR('',#8357,1.);
#2364=VECTOR('',#8358,1.);
#2365=VECTOR('',#8361,1.);
#2366=VECTOR('',#8362,1.);
#2367=VECTOR('',#8363,1.);
#2368=VECTOR('',#8366,1.);
#2369=VECTOR('',#8367,1.);
#2370=VECTOR('',#8384,0.325);
#2371=VECTOR('',#8389,0.35);
#2372=VECTOR('',#8394,0.335);
#2373=VECTOR('',#8403,0.21);
#2374=VECTOR('',#8406,0.2);
#2623=CIRCLE('',#6597,0.1954);
#2624=CIRCLE('',#6599,0.3);
#2625=CIRCLE('',#6601,0.35);
#2626=CIRCLE('',#6603,0.35);
#2627=CIRCLE('',#6605,0.32);
#2628=CIRCLE('',#6607,0.22);
#2629=CIRCLE('',#6609,0.1954);
#3048=VERTEX_POINT('',#9950);
#3049=VERTEX_POINT('',#9951);
#3050=VERTEX_POINT('',#9953);
#3051=VERTEX_POINT('',#9955);
#3052=VERTEX_POINT('',#9959);
#3053=VERTEX_POINT('',#9961);
#3054=VERTEX_POINT('',#9965);
#3055=VERTEX_POINT('',#9967);
#3056=VERTEX_POINT('',#9971);
#3057=VERTEX_POINT('',#9973);
#3058=VERTEX_POINT('',#9977);
#3059=VERTEX_POINT('',#9979);
#3060=VERTEX_POINT('',#9988);
#3061=VERTEX_POINT('',#9991);
#3062=VERTEX_POINT('',#9994);
#3063=VERTEX_POINT('',#9998);
#3064=VERTEX_POINT('',#10002);
#3065=VERTEX_POINT('',#10006);
#3066=VERTEX_POINT('',#10009);
#3708=EDGE_CURVE('',#3048,#3049,#1976,.T.);
#3709=EDGE_CURVE('',#3049,#3050,#1977,.T.);
#3710=EDGE_CURVE('',#3050,#3051,#1978,.T.);
#3711=EDGE_CURVE('',#3048,#3051,#1979,.T.);
#3712=EDGE_CURVE('',#3049,#3052,#1980,.T.);
#3713=EDGE_CURVE('',#3052,#3053,#1981,.T.);
#3714=EDGE_CURVE('',#3053,#3050,#1982,.T.);
#3715=EDGE_CURVE('',#3052,#3054,#1983,.T.);
#3716=EDGE_CURVE('',#3054,#3055,#1984,.T.);
#3717=EDGE_CURVE('',#3055,#3053,#1985,.T.);
#3718=EDGE_CURVE('',#3054,#3056,#1986,.T.);
#3719=EDGE_CURVE('',#3056,#3057,#1987,.T.);
#3720=EDGE_CURVE('',#3057,#3055,#1988,.T.);
#3721=EDGE_CURVE('',#3056,#3058,#1989,.T.);
#3722=EDGE_CURVE('',#3058,#3059,#1990,.T.);
#3723=EDGE_CURVE('',#3059,#3057,#1991,.T.);
#3724=EDGE_CURVE('',#3058,#3048,#1992,.T.);
#3725=EDGE_CURVE('',#3051,#3059,#1993,.T.);
#3726=EDGE_CURVE('',#3060,#3060,#2623,.T.);
#3727=EDGE_CURVE('',#3061,#3061,#2624,.T.);
#3728=EDGE_CURVE('',#3062,#3062,#2625,.T.);
#3729=EDGE_CURVE('',#3062,#3061,#1994,.T.);
#3730=EDGE_CURVE('',#3063,#3063,#2626,.T.);
#3731=EDGE_CURVE('',#3063,#3062,#1995,.T.);
#3732=EDGE_CURVE('',#3064,#3064,#2627,.T.);
#3733=EDGE_CURVE('',#3064,#3063,#1996,.T.);
#3734=EDGE_CURVE('',#3065,#3065,#2628,.T.);
#3735=EDGE_CURVE('',#3066,#3066,#2629,.F.);
#3736=EDGE_CURVE('',#3066,#3065,#1997,.T.);
#3737=EDGE_CURVE('',#3060,#3066,#1998,.T.);
#5020=ORIENTED_EDGE('',*,*,#3708,.T.);
#5021=ORIENTED_EDGE('',*,*,#3709,.T.);
#5022=ORIENTED_EDGE('',*,*,#3710,.T.);
#5023=ORIENTED_EDGE('',*,*,#3711,.F.);
#5024=ORIENTED_EDGE('',*,*,#3712,.T.);
#5025=ORIENTED_EDGE('',*,*,#3713,.T.);
#5026=ORIENTED_EDGE('',*,*,#3714,.T.);
#5027=ORIENTED_EDGE('',*,*,#3709,.F.);
#5028=ORIENTED_EDGE('',*,*,#3715,.T.);
#5029=ORIENTED_EDGE('',*,*,#3716,.T.);
#5030=ORIENTED_EDGE('',*,*,#3717,.T.);
#5031=ORIENTED_EDGE('',*,*,#3713,.F.);
#5032=ORIENTED_EDGE('',*,*,#3718,.T.);
#5033=ORIENTED_EDGE('',*,*,#3719,.T.);
#5034=ORIENTED_EDGE('',*,*,#3720,.T.);
#5035=ORIENTED_EDGE('',*,*,#3716,.F.);
#5036=ORIENTED_EDGE('',*,*,#3721,.T.);
#5037=ORIENTED_EDGE('',*,*,#3722,.T.);
#5038=ORIENTED_EDGE('',*,*,#3723,.T.);
#5039=ORIENTED_EDGE('',*,*,#3719,.F.);
#5040=ORIENTED_EDGE('',*,*,#3724,.T.);
#5041=ORIENTED_EDGE('',*,*,#3711,.T.);
#5042=ORIENTED_EDGE('',*,*,#3725,.T.);
#5043=ORIENTED_EDGE('',*,*,#3722,.F.);
#5044=ORIENTED_EDGE('',*,*,#3724,.F.);
#5045=ORIENTED_EDGE('',*,*,#3721,.F.);
#5046=ORIENTED_EDGE('',*,*,#3718,.F.);
#5047=ORIENTED_EDGE('',*,*,#3715,.F.);
#5048=ORIENTED_EDGE('',*,*,#3712,.F.);
#5049=ORIENTED_EDGE('',*,*,#3708,.F.);
#5050=ORIENTED_EDGE('',*,*,#3725,.F.);
#5051=ORIENTED_EDGE('',*,*,#3710,.F.);
#5052=ORIENTED_EDGE('',*,*,#3714,.F.);
#5053=ORIENTED_EDGE('',*,*,#3717,.F.);
#5054=ORIENTED_EDGE('',*,*,#3720,.F.);
#5055=ORIENTED_EDGE('',*,*,#3723,.F.);
#5056=ORIENTED_EDGE('',*,*,#3726,.F.);
#5057=ORIENTED_EDGE('',*,*,#3727,.F.);
#5058=ORIENTED_EDGE('',*,*,#3728,.F.);
#5059=ORIENTED_EDGE('',*,*,#3729,.T.);
#5060=ORIENTED_EDGE('',*,*,#3727,.T.);
#5061=ORIENTED_EDGE('',*,*,#3729,.F.);
#5062=ORIENTED_EDGE('',*,*,#3730,.F.);
#5063=ORIENTED_EDGE('',*,*,#3731,.T.);
#5064=ORIENTED_EDGE('',*,*,#3728,.T.);
#5065=ORIENTED_EDGE('',*,*,#3731,.F.);
#5066=ORIENTED_EDGE('',*,*,#3732,.F.);
#5067=ORIENTED_EDGE('',*,*,#3733,.T.);
#5068=ORIENTED_EDGE('',*,*,#3730,.T.);
#5069=ORIENTED_EDGE('',*,*,#3733,.F.);
#5070=ORIENTED_EDGE('',*,*,#3732,.T.);
#5071=ORIENTED_EDGE('',*,*,#3734,.F.);
#5072=ORIENTED_EDGE('',*,*,#3735,.F.);
#5073=ORIENTED_EDGE('',*,*,#3736,.T.);
#5074=ORIENTED_EDGE('',*,*,#3734,.T.);
#5075=ORIENTED_EDGE('',*,*,#3736,.F.);
#5076=ORIENTED_EDGE('',*,*,#3726,.T.);
#5077=ORIENTED_EDGE('',*,*,#3737,.T.);
#5078=ORIENTED_EDGE('',*,*,#3735,.T.);
#5079=ORIENTED_EDGE('',*,*,#3737,.F.);
#5182=CYLINDRICAL_SURFACE('',#6602,0.35);
#5183=CYLINDRICAL_SURFACE('',#6610,0.1954);
#5500=ADVANCED_FACE('',(#1151),#824,.F.);
#5501=ADVANCED_FACE('',(#1152),#825,.F.);
#5502=ADVANCED_FACE('',(#1153),#826,.F.);
#5503=ADVANCED_FACE('',(#1154),#827,.F.);
#5504=ADVANCED_FACE('',(#1155),#828,.F.);
#5505=ADVANCED_FACE('',(#1156),#829,.F.);
#5506=ADVANCED_FACE('',(#1157),#830,.F.);
#5507=ADVANCED_FACE('',(#1158),#831,.F.);
#5508=ADVANCED_FACE('',(#1159),#832,.F.);
#5509=ADVANCED_FACE('',(#1160),#833,.T.);
#5510=ADVANCED_FACE('',(#1161),#369,.T.);
#5511=ADVANCED_FACE('',(#1162),#5182,.T.);
#5512=ADVANCED_FACE('',(#1163),#370,.T.);
#5513=ADVANCED_FACE('',(#1164,#634),#834,.T.);
#5514=ADVANCED_FACE('',(#1165),#371,.T.);
#5515=ADVANCED_FACE('',(#1166),#5183,.T.);
#5550=CLOSED_SHELL('',(#5500,#5501,#5502,#5503,#5504,#5505,#5506,#5507));
#5551=CLOSED_SHELL('',(#5508,#5509,#5510,#5511,#5512,#5513,#5514,#5515));
#6587=AXIS2_PLACEMENT_3D('',#9948,#8336,#8337);
#6588=AXIS2_PLACEMENT_3D('',#9949,#8338,#8339);
#6589=AXIS2_PLACEMENT_3D('',#9958,#8344,#8345);
#6590=AXIS2_PLACEMENT_3D('',#9964,#8349,#8350);
#6591=AXIS2_PLACEMENT_3D('',#9970,#8354,#8355);
#6592=AXIS2_PLACEMENT_3D('',#9976,#8359,#8360);
#6593=AXIS2_PLACEMENT_3D('',#9982,#8364,#8365);
#6594=AXIS2_PLACEMENT_3D('',#9985,#8368,#8369);
#6595=AXIS2_PLACEMENT_3D('',#9986,#8370,#8371);
#6596=AXIS2_PLACEMENT_3D('',#9987,#8372,#8373);
#6597=AXIS2_PLACEMENT_3D('',#9989,#8374,#8375);
#6598=AXIS2_PLACEMENT_3D('',#9990,#8376,#8377);
#6599=AXIS2_PLACEMENT_3D('',#9992,#8378,#8379);
#6600=AXIS2_PLACEMENT_3D('',#9993,#8380,#8381);
#6601=AXIS2_PLACEMENT_3D('',#9995,#8382,#8383);
#6602=AXIS2_PLACEMENT_3D('',#9997,#8385,#8386);
#6603=AXIS2_PLACEMENT_3D('',#9999,#8387,#8388);
#6604=AXIS2_PLACEMENT_3D('',#10001,#8390,#8391);
#6605=AXIS2_PLACEMENT_3D('',#10003,#8392,#8393);
#6606=AXIS2_PLACEMENT_3D('',#10005,#8395,#8396);
#6607=AXIS2_PLACEMENT_3D('',#10007,#8397,#8398);
#6608=AXIS2_PLACEMENT_3D('',#10008,#8399,#8400);
#6609=AXIS2_PLACEMENT_3D('',#10010,#8401,#8402);
#6610=AXIS2_PLACEMENT_3D('',#10012,#8404,#8405);
#8336=DIRECTION('axis',(0.,0.,1.));
#8337=DIRECTION('refdir',(1.,0.,0.));
#8338=DIRECTION('center_axis',(0.866025403784439,0.,-0.5));
#8339=DIRECTION('ref_axis',(0.5,0.,0.866025403784439));
#8340=DIRECTION('',(-0.5,0.,-0.866025403784439));
#8341=DIRECTION('',(0.,-1.,0.));
#8342=DIRECTION('',(0.5,0.,0.866025403784439));
#8343=DIRECTION('',(0.,-1.,0.));
#8344=DIRECTION('center_axis',(1.60246890531964E-16,0.,-1.));
#8345=DIRECTION('ref_axis',(1.,0.,1.60246890531964E-16));
#8346=DIRECTION('',(-1.,0.,-1.60246890531964E-16));
#8347=DIRECTION('',(0.,-1.,0.));
#8348=DIRECTION('',(1.,0.,1.60246890531964E-16));
#8349=DIRECTION('center_axis',(-0.866025403784439,0.,-0.5));
#8350=DIRECTION('ref_axis',(0.5,0.,-0.866025403784439));
#8351=DIRECTION('',(-0.5,0.,0.866025403784439));
#8352=DIRECTION('',(0.,-1.,0.));
#8353=DIRECTION('',(0.5,0.,-0.866025403784439));
#8354=DIRECTION('center_axis',(-0.866025403784439,0.,0.5));
#8355=DIRECTION('ref_axis',(-0.5,0.,-0.866025403784439));
#8356=DIRECTION('',(0.5,0.,0.866025403784439));
#8357=DIRECTION('',(0.,-1.,0.));
#8358=DIRECTION('',(-0.5,0.,-0.866025403784439));
#8359=DIRECTION('center_axis',(-1.60246890531964E-16,0.,1.));
#8360=DIRECTION('ref_axis',(-1.,0.,-1.60246890531964E-16));
#8361=DIRECTION('',(1.,0.,1.60246890531964E-16));
#8362=DIRECTION('',(0.,-1.,0.));
#8363=DIRECTION('',(-1.,0.,-1.60246890531964E-16));
#8364=DIRECTION('center_axis',(0.866025403784439,0.,0.5));
#8365=DIRECTION('ref_axis',(-0.5,0.,0.866025403784439));
#8366=DIRECTION('',(0.5,0.,-0.866025403784439));
#8367=DIRECTION('',(-0.5,0.,0.866025403784439));
#8368=DIRECTION('center_axis',(0.,1.,0.));
#8369=DIRECTION('ref_axis',(1.,0.,0.));
#8370=DIRECTION('center_axis',(0.,-1.,0.));
#8371=DIRECTION('ref_axis',(0.,0.,-1.));
#8372=DIRECTION('center_axis',(0.,1.,0.));
#8373=DIRECTION('ref_axis',(1.,0.,0.));
#8374=DIRECTION('center_axis',(0.,1.,0.));
#8375=DIRECTION('ref_axis',(1.,0.,0.));
#8376=DIRECTION('center_axis',(0.,1.,0.));
#8377=DIRECTION('ref_axis',(0.,0.,1.));
#8378=DIRECTION('center_axis',(0.,-1.,0.));
#8379=DIRECTION('ref_axis',(1.,0.,0.));
#8380=DIRECTION('center_axis',(0.,-1.,0.));
#8381=DIRECTION('ref_axis',(1.,0.,0.));
#8382=DIRECTION('center_axis',(0.,-1.,0.));
#8383=DIRECTION('ref_axis',(1.,0.,0.));
#8384=DIRECTION('',(0.707106781186547,0.707106781186548,8.65956056235493E-17));
#8385=DIRECTION('center_axis',(0.,-1.,0.));
#8386=DIRECTION('ref_axis',(1.,0.,0.));
#8387=DIRECTION('center_axis',(0.,-1.,0.));
#8388=DIRECTION('ref_axis',(1.,0.,0.));
#8389=DIRECTION('',(0.,1.,0.));
#8390=DIRECTION('center_axis',(0.,1.,0.));
#8391=DIRECTION('ref_axis',(1.,0.,0.));
#8392=DIRECTION('center_axis',(0.,-1.,0.));
#8393=DIRECTION('ref_axis',(1.,0.,0.));
#8394=DIRECTION('',(-0.707106781186547,0.707106781186548,-8.65956056235493E-17));
#8395=DIRECTION('center_axis',(0.,-1.,0.));
#8396=DIRECTION('ref_axis',(0.,0.,-1.));
#8397=DIRECTION('center_axis',(0.,-1.,0.));
#8398=DIRECTION('ref_axis',(1.,0.,0.));
#8399=DIRECTION('center_axis',(0.,1.,0.));
#8400=DIRECTION('ref_axis',(1.,0.,0.));
#8401=DIRECTION('center_axis',(0.,1.,0.));
#8402=DIRECTION('ref_axis',(1.,0.,0.));
#8403=DIRECTION('',(-0.447213595499958,0.894427190999916,-5.47678698264203E-17));
#8404=DIRECTION('center_axis',(0.,-1.,0.));
#8405=DIRECTION('ref_axis',(1.,0.,0.));
#8406=DIRECTION('',(0.,1.,0.));
#9948=CARTESIAN_POINT('',(0.,0.,0.));
#9949=CARTESIAN_POINT('Origin',(0.0866025403784439,-0.4,-0.15));
#9950=CARTESIAN_POINT('',(0.173205080756888,-0.4,0.));
#9951=CARTESIAN_POINT('',(0.0866025403784439,-0.4,-0.15));
#9952=CARTESIAN_POINT('',(0.173205080756888,-0.4,0.));
#9953=CARTESIAN_POINT('',(0.0866025403784439,-0.64,-0.15));
#9954=CARTESIAN_POINT('',(0.0866025403784439,-0.4,-0.15));
#9955=CARTESIAN_POINT('',(0.173205080756888,-0.64,0.));
#9956=CARTESIAN_POINT('',(0.173205080756888,-0.64,0.));
#9957=CARTESIAN_POINT('',(0.173205080756888,-0.4,0.));
#9958=CARTESIAN_POINT('Origin',(-0.0866025403784438,-0.4,-0.15));
#9959=CARTESIAN_POINT('',(-0.0866025403784438,-0.4,-0.15));
#9960=CARTESIAN_POINT('',(0.0866025403784439,-0.4,-0.15));
#9961=CARTESIAN_POINT('',(-0.0866025403784438,-0.64,-0.15));
#9962=CARTESIAN_POINT('',(-0.0866025403784438,-0.4,-0.15));
#9963=CARTESIAN_POINT('',(0.0866025403784439,-0.64,-0.15));
#9964=CARTESIAN_POINT('Origin',(-0.173205080756888,-0.4,-2.77555756156289E-17));
#9965=CARTESIAN_POINT('',(-0.173205080756888,-0.4,-2.12115047744981E-17));
#9966=CARTESIAN_POINT('',(-0.0866025403784438,-0.4,-0.15));
#9967=CARTESIAN_POINT('',(-0.173205080756888,-0.64,-2.77555756156289E-17));
#9968=CARTESIAN_POINT('',(-0.173205080756888,-0.4,-2.12115047744981E-17));
#9969=CARTESIAN_POINT('',(-0.0866025403784438,-0.64,-0.15));
#9970=CARTESIAN_POINT('Origin',(-0.0866025403784439,-0.4,0.15));
#9971=CARTESIAN_POINT('',(-0.0866025403784439,-0.4,0.15));
#9972=CARTESIAN_POINT('',(-0.173205080756888,-0.4,-2.12115047744981E-17));
#9973=CARTESIAN_POINT('',(-0.0866025403784439,-0.64,0.15));
#9974=CARTESIAN_POINT('',(-0.0866025403784439,-0.4,0.15));
#9975=CARTESIAN_POINT('',(-0.173205080756888,-0.64,-2.12115047744981E-17));
#9976=CARTESIAN_POINT('Origin',(0.0866025403784439,-0.4,0.15));
#9977=CARTESIAN_POINT('',(0.0866025403784439,-0.4,0.15));
#9978=CARTESIAN_POINT('',(-0.0866025403784439,-0.4,0.15));
#9979=CARTESIAN_POINT('',(0.0866025403784439,-0.64,0.15));
#9980=CARTESIAN_POINT('',(0.0866025403784439,-0.4,0.15));
#9981=CARTESIAN_POINT('',(-0.0866025403784439,-0.64,0.15));
#9982=CARTESIAN_POINT('Origin',(0.173205080756888,-0.4,0.));
#9983=CARTESIAN_POINT('',(0.0866025403784439,-0.4,0.15));
#9984=CARTESIAN_POINT('',(0.0866025403784439,-0.64,0.15));
#9985=CARTESIAN_POINT('Origin',(0.,-0.4,-2.77555756156289E-17));
#9986=CARTESIAN_POINT('Origin',(0.,-0.64,-2.77555756156289E-17));
#9987=CARTESIAN_POINT('Origin',(0.,-1.,0.));
#9988=CARTESIAN_POINT('',(-0.1954,-1.,2.39295984553393E-17));
#9989=CARTESIAN_POINT('Origin',(0.,-1.,0.));
#9990=CARTESIAN_POINT('Origin',(0.3,0.4,0.));
#9991=CARTESIAN_POINT('',(-0.3,0.4,-3.67394039744206E-17));
#9992=CARTESIAN_POINT('Origin',(0.,0.4,0.));
#9993=CARTESIAN_POINT('Origin',(0.,0.375,0.));
#9994=CARTESIAN_POINT('',(-0.35,0.35,-4.28626379701573E-17));
#9995=CARTESIAN_POINT('Origin',(0.,0.35,0.));
#9996=CARTESIAN_POINT('',(-0.325,0.375,-3.9801020972289E-17));
#9997=CARTESIAN_POINT('Origin',(0.,0.19,0.));
#9998=CARTESIAN_POINT('',(-0.35,0.03,-4.28626379701574E-17));
#9999=CARTESIAN_POINT('Origin',(0.,0.03,0.));
#10000=CARTESIAN_POINT('',(-0.35,0.19,-4.28626379701574E-17));
#10001=CARTESIAN_POINT('Origin',(0.,0.0149999999999999,0.));
#10002=CARTESIAN_POINT('',(-0.32,-3.29597460435593E-17,-3.91886975727153E-17));
#10003=CARTESIAN_POINT('Origin',(0.,0.,0.));
#10004=CARTESIAN_POINT('',(-0.335,0.0149999999999999,-4.10256677714363E-17));
#10005=CARTESIAN_POINT('Origin',(0.22,0.,0.));
#10006=CARTESIAN_POINT('',(-0.22,-6.93889390390723E-18,-2.69422295812418E-17));
#10007=CARTESIAN_POINT('Origin',(0.,0.,0.));
#10008=CARTESIAN_POINT('Origin',(0.,-0.02,0.));
#10009=CARTESIAN_POINT('',(-0.1954,-0.0492,2.39295984553393E-17));
#10010=CARTESIAN_POINT('Origin',(0.,-0.0492,0.));
#10011=CARTESIAN_POINT('',(-0.21,-0.02,-2.57175827820944E-17));
#10012=CARTESIAN_POINT('Origin',(0.,-0.8,0.));
#10013=CARTESIAN_POINT('',(-0.1954,-0.8,-2.39295984553393E-17));
#10057=UNCERTAINTY_MEASURE_WITH_UNIT(LENGTH_MEASURE(0.001),#10096,
'DISTANCE_ACCURACY_VALUE',
'Maximum model space distance between geometric entities at asserted c
onnectivities');
#10058=UNCERTAINTY_MEASURE_WITH_UNIT(LENGTH_MEASURE(0.001),#10096,
'DISTANCE_ACCURACY_VALUE',
'Maximum model space distance between geometric entities at asserted c
onnectivities');
#10094=(
GEOMETRIC_REPRESENTATION_CONTEXT(3)
GLOBAL_UNCERTAINTY_ASSIGNED_CONTEXT((#10057))
GLOBAL_UNIT_ASSIGNED_CONTEXT((#10096,#10098,#10099))
REPRESENTATION_CONTEXT('','3D')
);
#10095=(
GEOMETRIC_REPRESENTATION_CONTEXT(3)
GLOBAL_UNCERTAINTY_ASSIGNED_CONTEXT((#10058))
GLOBAL_UNIT_ASSIGNED_CONTEXT((#10096,#10098,#10099))
REPRESENTATION_CONTEXT('','3D')
);
#10096=(
LENGTH_UNIT()
NAMED_UNIT(*)
SI_UNIT(.CENTI.,.METRE.)
);
#10098=(
NAMED_UNIT(*)
PLANE_ANGLE_UNIT()
SI_UNIT($,.RADIAN.)
);
#10099=(
NAMED_UNIT(*)
SI_UNIT($,.STERADIAN.)
SOLID_ANGLE_UNIT()
);
#10135=SHAPE_DEFINITION_REPRESENTATION(#10238,#10282);
#10238=PRODUCT_DEFINITION_SHAPE('',$,#10319);
#10282=SHAPE_REPRESENTATION('',(#6587),#10094);
#10283=PRODUCT_DEFINITION_CONTEXT('part definition',#10393,'design');
#10319=PRODUCT_DEFINITION('M4x10 Cap Screw','M4x10 Cap Screw',#10355,#10283);
#10355=PRODUCT_DEFINITION_FORMATION('',$,#10430);
#10393=APPLICATION_CONTEXT(
'Core Data for Automotive Mechanical Design Process');
#10394=PRODUCT_CONTEXT('part definition',#10393,'mechanical');
#10430=PRODUCT('M4x10 Cap Screw','M4x10 Cap Screw','M4x10 Cap Screw',(#10394));
#10501=COLOUR_RGB('Black',0.12,0.14,0.17);
#10502=FILL_AREA_STYLE_COLOUR('',#10501);
#10503=FILL_AREA_STYLE('',(#10502));
#10504=SURFACE_STYLE_FILL_AREA(#10503);
#10505=SURFACE_SIDE_STYLE('',(#10504));
#10506=SURFACE_STYLE_USAGE(.BOTH.,#10505);
#10507=PRESENTATION_STYLE_ASSIGNMENT((#10506));
ENDSEC;
END-ISO-10303-21;
